ISO-10303-21;
HEADER;
/* Generated by software containing ST-Developer
 * from STEP Tools, Inc. (www.steptools.com) 
 */

FILE_DESCRIPTION(
/* description */ ('Twin-shaft manual slide'),
/* implementation_level */ '2;1');

FILE_NAME(
/* name */ 'Cap Screw - M4x16.step',
/* time_stamp */ '2026-10-27T18:38:08-07:00',
/* author */ (''),
/* organization */ (''),
/* preprocessor_version */ 'ST-DEVELOPER v20.2',
/* originating_system */ 'Autodesk Translation Framework v15.17.0.0',
/* authorisation */ '');

FILE_SCHEMA (('AUTOMOTIVE_DESIGN { 1 0 10303 214 3 1 1 }'));
ENDSEC;

DATA;
#10=MECHANICAL_DESIGN_GEOMETRIC_PRESENTATION_REPRESENTATION('',(#287),#6463);
#220=ORIENTED_CLOSED_SHELL('',*,#3651,.F.);
#224=BREP_WITH_VOIDS('Body1',#3650,(#220));
#232=CONICAL_SURFACE('',#4124,0.325,0.785398163397448);
#233=CONICAL_SURFACE('',#4128,0.335,0.785398163397448);
#234=CONICAL_SURFACE('',#4132,0.21,0.463647609000806);
#235=CONICAL_SURFACE('',#4136,0.18,0.785398163397448);
#255=SHAPE_REPRESENTATION_RELATIONSHIP('SRR','None',#6575,#271);
#271=ADVANCED_BREP_SHAPE_REPRESENTATION('',(#224),#6458);
#287=STYLED_ITEM('',(#6747),#224);
#394=FACE_BOUND('',#976,.T.);
#489=PLANE('',#4122);
#490=PLANE('',#4130);
#491=PLANE('',#4138);
#492=PLANE('',#4139);
#493=PLANE('',#4140);
#494=PLANE('',#4141);
#495=PLANE('',#4142);
#496=PLANE('',#4143);
#497=PLANE('',#4144);
#498=PLANE('',#4145);
#499=PLANE('',#4146);
#674=FACE_OUTER_BOUND('',#971,.T.);
#675=FACE_OUTER_BOUND('',#972,.T.);
#676=FACE_OUTER_BOUND('',#973,.T.);
#677=FACE_OUTER_BOUND('',#974,.T.);
#678=FACE_OUTER_BOUND('',#975,.T.);
#679=FACE_OUTER_BOUND('',#977,.T.);
#680=FACE_OUTER_BOUND('',#978,.T.);
#681=FACE_OUTER_BOUND('',#979,.T.);
#682=FACE_OUTER_BOUND('',#980,.T.);
#683=FACE_OUTER_BOUND('',#981,.T.);
#684=FACE_OUTER_BOUND('',#982,.T.);
#685=FACE_OUTER_BOUND('',#983,.T.);
#686=FACE_OUTER_BOUND('',#984,.T.);
#687=FACE_OUTER_BOUND('',#985,.T.);
#688=FACE_OUTER_BOUND('',#986,.T.);
#689=FACE_OUTER_BOUND('',#987,.T.);
#690=FACE_OUTER_BOUND('',#988,.T.);
#971=EDGE_LOOP('',(#3150));
#972=EDGE_LOOP('',(#3151,#3152,#3153,#3154));
#973=EDGE_LOOP('',(#3155,#3156,#3157,#3158));
#974=EDGE_LOOP('',(#3159,#3160,#3161,#3162));
#975=EDGE_LOOP('',(#3163));
#976=EDGE_LOOP('',(#3164));
#977=EDGE_LOOP('',(#3165,#3166,#3167,#3168));
#978=EDGE_LOOP('',(#3169,#3170,#3171,#3172));
#979=EDGE_LOOP('',(#3173,#3174,#3175,#3176));
#980=EDGE_LOOP('',(#3177));
#981=EDGE_LOOP('',(#3178,#3179,#3180,#3181));
#982=EDGE_LOOP('',(#3182,#3183,#3184,#3185));
#983=EDGE_LOOP('',(#3186,#3187,#3188,#3189));
#984=EDGE_LOOP('',(#3190,#3191,#3192,#3193));
#985=EDGE_LOOP('',(#3194,#3195,#3196,#3197));
#986=EDGE_LOOP('',(#3198,#3199,#3200,#3201));
#987=EDGE_LOOP('',(#3202,#3203,#3204,#3205,#3206,#3207));
#988=EDGE_LOOP('',(#3208,#3209,#3210,#3211,#3212,#3213));
#1247=LINE('',#6139,#1533);
#1248=LINE('',#6143,#1534);
#1249=LINE('',#6147,#1535);
#1250=LINE('',#6154,#1536);
#1251=LINE('',#6158,#1537);
#1252=LINE('',#6162,#1538);
#1253=LINE('',#6167,#1539);
#1254=LINE('',#6169,#1540);
#1255=LINE('',#6171,#1541);
#1256=LINE('',#6172,#1542);
#1257=LINE('',#6175,#1543);
#1258=LINE('',#6177,#1544);
#1259=LINE('',#6178,#1545);
#1260=LINE('',#6181,#1546);
#1261=LINE('',#6183,#1547);
#1262=LINE('',#6184,#1548);
#1263=LINE('',#6187,#1549);
#1264=LINE('',#6189,#1550);
#1265=LINE('',#6190,#1551);
#1266=LINE('',#6193,#1552);
#1267=LINE('',#6195,#1553);
#1268=LINE('',#6196,#1554);
#1269=LINE('',#6198,#1555);
#1270=LINE('',#6199,#1556);
#1533=VECTOR('',#5059,0.325);
#1534=VECTOR('',#5064,0.35);
#1535=VECTOR('',#5069,0.335);
#1536=VECTOR('',#5078,0.21);
#1537=VECTOR('',#5083,0.2);
#1538=VECTOR('',#5088,0.18);
#1539=VECTOR('',#5093,1.);
#1540=VECTOR('',#5094,1.);
#1541=VECTOR('',#5095,1.);
#1542=VECTOR('',#5096,1.);
#1543=VECTOR('',#5099,1.);
#1544=VECTOR('',#5100,1.);
#1545=VECTOR('',#5101,1.);
#1546=VECTOR('',#5104,1.);
#1547=VECTOR('',#5105,1.);
#1548=VECTOR('',#5106,1.);
#1549=VECTOR('',#5109,1.);
#1550=VECTOR('',#5110,1.);
#1551=VECTOR('',#5111,1.);
#1552=VECTOR('',#5114,1.);
#1553=VECTOR('',#5115,1.);
#1554=VECTOR('',#5116,1.);
#1555=VECTOR('',#5119,1.);
#1556=VECTOR('',#5120,1.);
#1730=CIRCLE('',#4123,0.3);
#1731=CIRCLE('',#4125,0.35);
#1732=CIRCLE('',#4127,0.35);
#1733=CIRCLE('',#4129,0.32);
#1734=CIRCLE('',#4131,0.22);
#1735=CIRCLE('',#4133,0.1954);
#1736=CIRCLE('',#4135,0.1954);
#1737=CIRCLE('',#4137,0.16);
#1981=VERTEX_POINT('',#6134);
#1982=VERTEX_POINT('',#6137);
#1983=VERTEX_POINT('',#6141);
#1984=VERTEX_POINT('',#6145);
#1985=VERTEX_POINT('',#6149);
#1986=VERTEX_POINT('',#6152);
#1987=VERTEX_POINT('',#6156);
#1988=VERTEX_POINT('',#6160);
#1989=VERTEX_POINT('',#6165);
#1990=VERTEX_POINT('',#6166);
#1991=VERTEX_POINT('',#6168);
#1992=VERTEX_POINT('',#6170);
#1993=VERTEX_POINT('',#6174);
#1994=VERTEX_POINT('',#6176);
#1995=VERTEX_POINT('',#6180);
#1996=VERTEX_POINT('',#6182);
#1997=VERTEX_POINT('',#6186);
#1998=VERTEX_POINT('',#6188);
#1999=VERTEX_POINT('',#6192);
#2000=VERTEX_POINT('',#6194);
#2380=EDGE_CURVE('',#1981,#1981,#1730,.T.);
#2381=EDGE_CURVE('',#1982,#1982,#1731,.T.);
#2382=EDGE_CURVE('',#1982,#1981,#1247,.T.);
#2383=EDGE_CURVE('',#1983,#1983,#1732,.T.);
#2384=EDGE_CURVE('',#1983,#1982,#1248,.T.);
#2385=EDGE_CURVE('',#1984,#1984,#1733,.T.);
#2386=EDGE_CURVE('',#1984,#1983,#1249,.T.);
#2387=EDGE_CURVE('',#1985,#1985,#1734,.T.);
#2388=EDGE_CURVE('',#1986,#1986,#1735,.F.);
#2389=EDGE_CURVE('',#1986,#1985,#1250,.T.);
#2390=EDGE_CURVE('',#1987,#1987,#1736,.F.);
#2391=EDGE_CURVE('',#1987,#1986,#1251,.T.);
#2392=EDGE_CURVE('',#1988,#1988,#1737,.T.);
#2393=EDGE_CURVE('',#1988,#1987,#1252,.T.);
#2394=EDGE_CURVE('',#1989,#1990,#1253,.T.);
#2395=EDGE_CURVE('',#1990,#1991,#1254,.T.);
#2396=EDGE_CURVE('',#1991,#1992,#1255,.T.);
#2397=EDGE_CURVE('',#1989,#1992,#1256,.T.);
#2398=EDGE_CURVE('',#1990,#1993,#1257,.T.);
#2399=EDGE_CURVE('',#1993,#1994,#1258,.T.);
#2400=EDGE_CURVE('',#1994,#1991,#1259,.T.);
#2401=EDGE_CURVE('',#1993,#1995,#1260,.T.);
#2402=EDGE_CURVE('',#1995,#1996,#1261,.T.);
#2403=EDGE_CURVE('',#1996,#1994,#1262,.T.);
#2404=EDGE_CURVE('',#1995,#1997,#1263,.T.);
#2405=EDGE_CURVE('',#1997,#1998,#1264,.T.);
#2406=EDGE_CURVE('',#1998,#1996,#1265,.T.);
#2407=EDGE_CURVE('',#1997,#1999,#1266,.T.);
#2408=EDGE_CURVE('',#1999,#2000,#1267,.T.);
#2409=EDGE_CURVE('',#2000,#1998,#1268,.T.);
#2410=EDGE_CURVE('',#1999,#1989,#1269,.T.);
#2411=EDGE_CURVE('',#1992,#2000,#1270,.T.);
#3150=ORIENTED_EDGE('',*,*,#2380,.F.);
#3151=ORIENTED_EDGE('',*,*,#2381,.F.);
#3152=ORIENTED_EDGE('',*,*,#2382,.T.);
#3153=ORIENTED_EDGE('',*,*,#2380,.T.);
#3154=ORIENTED_EDGE('',*,*,#2382,.F.);
#3155=ORIENTED_EDGE('',*,*,#2383,.F.);
#3156=ORIENTED_EDGE('',*,*,#2384,.T.);
#3157=ORIENTED_EDGE('',*,*,#2381,.T.);
#3158=ORIENTED_EDGE('',*,*,#2384,.F.);
#3159=ORIENTED_EDGE('',*,*,#2385,.F.);
#3160=ORIENTED_EDGE('',*,*,#2386,.T.);
#3161=ORIENTED_EDGE('',*,*,#2383,.T.);
#3162=ORIENTED_EDGE('',*,*,#2386,.F.);
#3163=ORIENTED_EDGE('',*,*,#2385,.T.);
#3164=ORIENTED_EDGE('',*,*,#2387,.F.);
#3165=ORIENTED_EDGE('',*,*,#2388,.F.);
#3166=ORIENTED_EDGE('',*,*,#2389,.T.);
#3167=ORIENTED_EDGE('',*,*,#2387,.T.);
#3168=ORIENTED_EDGE('',*,*,#2389,.F.);
#3169=ORIENTED_EDGE('',*,*,#2390,.F.);
#3170=ORIENTED_EDGE('',*,*,#2391,.T.);
#3171=ORIENTED_EDGE('',*,*,#2388,.T.);
#3172=ORIENTED_EDGE('',*,*,#2391,.F.);
#3173=ORIENTED_EDGE('',*,*,#2392,.F.);
#3174=ORIENTED_EDGE('',*,*,#2393,.T.);
#3175=ORIENTED_EDGE('',*,*,#2390,.T.);
#3176=ORIENTED_EDGE('',*,*,#2393,.F.);
#3177=ORIENTED_EDGE('',*,*,#2392,.T.);
#3178=ORIENTED_EDGE('',*,*,#2394,.T.);
#3179=ORIENTED_EDGE('',*,*,#2395,.T.);
#3180=ORIENTED_EDGE('',*,*,#2396,.T.);
#3181=ORIENTED_EDGE('',*,*,#2397,.F.);
#3182=ORIENTED_EDGE('',*,*,#2398,.T.);
#3183=ORIENTED_EDGE('',*,*,#2399,.T.);
#3184=ORIENTED_EDGE('',*,*,#2400,.T.);
#3185=ORIENTED_EDGE('',*,*,#2395,.F.);
#3186=ORIENTED_EDGE('',*,*,#2401,.T.);
#3187=ORIENTED_EDGE('',*,*,#2402,.T.);
#3188=ORIENTED_EDGE('',*,*,#2403,.T.);
#3189=ORIENTED_EDGE('',*,*,#2399,.F.);
#3190=ORIENTED_EDGE('',*,*,#2404,.T.);
#3191=ORIENTED_EDGE('',*,*,#2405,.T.);
#3192=ORIENTED_EDGE('',*,*,#2406,.T.);
#3193=ORIENTED_EDGE('',*,*,#2402,.F.);
#3194=ORIENTED_EDGE('',*,*,#2407,.T.);
#3195=ORIENTED_EDGE('',*,*,#2408,.T.);
#3196=ORIENTED_EDGE('',*,*,#2409,.T.);
#3197=ORIENTED_EDGE('',*,*,#2405,.F.);
#3198=ORIENTED_EDGE('',*,*,#2410,.T.);
#3199=ORIENTED_EDGE('',*,*,#2397,.T.);
#3200=ORIENTED_EDGE('',*,*,#2411,.T.);
#3201=ORIENTED_EDGE('',*,*,#2408,.F.);
#3202=ORIENTED_EDGE('',*,*,#2410,.F.);
#3203=ORIENTED_EDGE('',*,*,#2407,.F.);
#3204=ORIENTED_EDGE('',*,*,#2404,.F.);
#3205=ORIENTED_EDGE('',*,*,#2401,.F.);
#3206=ORIENTED_EDGE('',*,*,#2398,.F.);
#3207=ORIENTED_EDGE('',*,*,#2394,.F.);
#3208=ORIENTED_EDGE('',*,*,#2411,.F.);
#3209=ORIENTED_EDGE('',*,*,#2396,.F.);
#3210=ORIENTED_EDGE('',*,*,#2400,.F.);
#3211=ORIENTED_EDGE('',*,*,#2403,.F.);
#3212=ORIENTED_EDGE('',*,*,#2406,.F.);
#3213=ORIENTED_EDGE('',*,*,#2409,.F.);
#3421=CYLINDRICAL_SURFACE('',#4126,0.35);
#3422=CYLINDRICAL_SURFACE('',#4134,0.1954);
#3579=ADVANCED_FACE('',(#674),#489,.T.);
#3580=ADVANCED_FACE('',(#675),#232,.T.);
#3581=ADVANCED_FACE('',(#676),#3421,.T.);
#3582=ADVANCED_FACE('',(#677),#233,.T.);
#3583=ADVANCED_FACE('',(#678,#394),#490,.T.);
#3584=ADVANCED_FACE('',(#679),#234,.T.);
#3585=ADVANCED_FACE('',(#680),#3422,.T.);
#3586=ADVANCED_FACE('',(#681),#235,.T.);
#3587=ADVANCED_FACE('',(#682),#491,.T.);
#3588=ADVANCED_FACE('',(#683),#492,.F.);
#3589=ADVANCED_FACE('',(#684),#493,.F.);
#3590=ADVANCED_FACE('',(#685),#494,.F.);
#3591=ADVANCED_FACE('',(#686),#495,.F.);
#3592=ADVANCED_FACE('',(#687),#496,.F.);
#3593=ADVANCED_FACE('',(#688),#497,.F.);
#3594=ADVANCED_FACE('',(#689),#498,.F.);
#3595=ADVANCED_FACE('',(#690),#499,.F.);
#3650=CLOSED_SHELL('',(#3579,#3580,#3581,#3582,#3583,#3584,#3585,#3586,
#3587));
#3651=CLOSED_SHELL('',(#3588,#3589,#3590,#3591,#3592,#3593,#3594,#3595));
#4121=AXIS2_PLACEMENT_3D('',#6132,#5049,#5050);
#4122=AXIS2_PLACEMENT_3D('',#6133,#5051,#5052);
#4123=AXIS2_PLACEMENT_3D('',#6135,#5053,#5054);
#4124=AXIS2_PLACEMENT_3D('',#6136,#5055,#5056);
#4125=AXIS2_PLACEMENT_3D('',#6138,#5057,#5058);
#4126=AXIS2_PLACEMENT_3D('',#6140,#5060,#5061);
#4127=AXIS2_PLACEMENT_3D('',#6142,#5062,#5063);
#4128=AXIS2_PLACEMENT_3D('',#6144,#5065,#5066);
#4129=AXIS2_PLACEMENT_3D('',#6146,#5067,#5068);
#4130=AXIS2_PLACEMENT_3D('',#6148,#5070,#5071);
#4131=AXIS2_PLACEMENT_3D('',#6150,#5072,#5073);
#4132=AXIS2_PLACEMENT_3D('',#6151,#5074,#5075);
#4133=AXIS2_PLACEMENT_3D('',#6153,#5076,#5077);
#4134=AXIS2_PLACEMENT_3D('',#6155,#5079,#5080);
#4135=AXIS2_PLACEMENT_3D('',#6157,#5081,#5082);
#4136=AXIS2_PLACEMENT_3D('',#6159,#5084,#5085);
#4137=AXIS2_PLACEMENT_3D('',#6161,#5086,#5087);
#4138=AXIS2_PLACEMENT_3D('',#6163,#5089,#5090);
#4139=AXIS2_PLACEMENT_3D('',#6164,#5091,#5092);
#4140=AXIS2_PLACEMENT_3D('',#6173,#5097,#5098);
#4141=AXIS2_PLACEMENT_3D('',#6179,#5102,#5103);
#4142=AXIS2_PLACEMENT_3D('',#6185,#5107,#5108);
#4143=AXIS2_PLACEMENT_3D('',#6191,#5112,#5113);
#4144=AXIS2_PLACEMENT_3D('',#6197,#5117,#5118);
#4145=AXIS2_PLACEMENT_3D('',#6200,#5121,#5122);
#4146=AXIS2_PLACEMENT_3D('',#6201,#5123,#5124);
#5049=DIRECTION('axis',(0.,0.,1.));
#5050=DIRECTION('refdir',(1.,0.,0.));
#5051=DIRECTION('center_axis',(0.,1.,0.));
#5052=DIRECTION('ref_axis',(0.,0.,1.));
#5053=DIRECTION('center_axis',(0.,-1.,0.));
#5054=DIRECTION('ref_axis',(1.,0.,0.));
#5055=DIRECTION('center_axis',(0.,-1.,0.));
#5056=DIRECTION('ref_axis',(1.,0.,0.));
#5057=DIRECTION('center_axis',(0.,-1.,0.));
#5058=DIRECTION('ref_axis',(1.,0.,0.));
#5059=DIRECTION('',(0.707106781186547,0.707106781186548,8.65956056235493E-17));
#5060=DIRECTION('center_axis',(0.,-1.,0.));
#5061=DIRECTION('ref_axis',(1.,0.,0.));
#5062=DIRECTION('center_axis',(0.,-1.,0.));
#5063=DIRECTION('ref_axis',(1.,0.,0.));
#5064=DIRECTION('',(0.,1.,0.));
#5065=DIRECTION('center_axis',(0.,1.,0.));
#5066=DIRECTION('ref_axis',(1.,0.,0.));
#5067=DIRECTION('center_axis',(0.,-1.,0.));
#5068=DIRECTION('ref_axis',(1.,0.,0.));
#5069=DIRECTION('',(-0.707106781186547,0.707106781186548,-8.65956056235493E-17));
#5070=DIRECTION('center_axis',(0.,-1.,0.));
#5071=DIRECTION('ref_axis',(0.,0.,-1.));
#5072=DIRECTION('center_axis',(0.,-1.,0.));
#5073=DIRECTION('ref_axis',(1.,0.,0.));
#5074=DIRECTION('center_axis',(0.,1.,0.));
#5075=DIRECTION('ref_axis',(1.,0.,0.));
#5076=DIRECTION('center_axis',(0.,1.,0.));
#5077=DIRECTION('ref_axis',(1.,0.,0.));
#5078=DIRECTION('',(-0.447213595499958,0.894427190999916,-5.47678698264203E-17));
#5079=DIRECTION('center_axis',(0.,-1.,0.));
#5080=DIRECTION('ref_axis',(1.,0.,0.));
#5081=DIRECTION('center_axis',(0.,1.,0.));
#5082=DIRECTION('ref_axis',(1.,0.,0.));
#5083=DIRECTION('',(0.,1.,0.));
#5084=DIRECTION('center_axis',(0.,1.,0.));
#5085=DIRECTION('ref_axis',(1.,0.,0.));
#5086=DIRECTION('center_axis',(0.,-1.,0.));
#5087=DIRECTION('ref_axis',(1.,0.,0.));
#5088=DIRECTION('',(-0.707106781186547,0.707106781186548,-8.65956056235493E-17));
#5089=DIRECTION('center_axis',(0.,-1.,0.));
#5090=DIRECTION('ref_axis',(0.,0.,-1.));
#5091=DIRECTION('center_axis',(0.866025403784439,0.,-0.5));
#5092=DIRECTION('ref_axis',(0.5,0.,0.866025403784439));
#5093=DIRECTION('',(-0.5,0.,-0.866025403784439));
#5094=DIRECTION('',(0.,-1.,0.));
#5095=DIRECTION('',(0.5,0.,0.866025403784439));
#5096=DIRECTION('',(0.,-1.,0.));
#5097=DIRECTION('center_axis',(1.60246890531964E-16,0.,-1.));
#5098=DIRECTION('ref_axis',(1.,0.,1.60246890531964E-16));
#5099=DIRECTION('',(-1.,0.,-1.60246890531964E-16));
#5100=DIRECTION('',(0.,-1.,0.));
#5101=DIRECTION('',(1.,0.,1.60246890531964E-16));
#5102=DIRECTION('center_axis',(-0.866025403784439,0.,-0.5));
#5103=DIRECTION('ref_axis',(0.5,0.,-0.866025403784439));
#5104=DIRECTION('',(-0.5,0.,0.866025403784439));
#5105=DIRECTION('',(0.,-1.,0.));
#5106=DIRECTION('',(0.5,0.,-0.866025403784439));
#5107=DIRECTION('center_axis',(-0.866025403784439,0.,0.5));
#5108=DIRECTION('ref_axis',(-0.5,0.,-0.866025403784439));
#5109=DIRECTION('',(0.5,0.,0.866025403784439));
#5110=DIRECTION('',(0.,-1.,0.));
#5111=DIRECTION('',(-0.5,0.,-0.866025403784439));
#5112=DIRECTION('center_axis',(-1.60246890531964E-16,0.,1.));
#5113=DIRECTION('ref_axis',(-1.,0.,-1.60246890531964E-16));
#5114=DIRECTION('',(1.,0.,1.60246890531964E-16));
#5115=DIRECTION('',(0.,-1.,0.));
#5116=DIRECTION('',(-1.,0.,-1.60246890531964E-16));
#5117=DIRECTION('center_axis',(0.866025403784439,0.,0.5));
#5118=DIRECTION('ref_axis',(-0.5,0.,0.866025403784439));
#5119=DIRECTION('',(0.5,0.,-0.866025403784439));
#5120=DIRECTION('',(-0.5,0.,0.866025403784439));
#5121=DIRECTION('center_axis',(0.,1.,0.));
#5122=DIRECTION('ref_axis',(1.,0.,0.));
#5123=DIRECTION('center_axis',(0.,-1.,0.));
#5124=DIRECTION('ref_axis',(0.,0.,-1.));
#6132=CARTESIAN_POINT('',(0.,0.,0.));
#6133=CARTESIAN_POINT('Origin',(0.3,0.4,0.));
#6134=CARTESIAN_POINT('',(-0.3,0.4,-3.67394039744206E-17));
#6135=CARTESIAN_POINT('Origin',(0.,0.4,0.));
#6136=CARTESIAN_POINT('Origin',(0.,0.375,0.));
#6137=CARTESIAN_POINT('',(-0.35,0.35,-4.28626379701573E-17));
#6138=CARTESIAN_POINT('Origin',(0.,0.35,0.));
#6139=CARTESIAN_POINT('',(-0.325,0.375,-3.9801020972289E-17));
#6140=CARTESIAN_POINT('Origin',(0.,0.19,0.));
#6141=CARTESIAN_POINT('',(-0.35,0.03,-4.28626379701574E-17));
#6142=CARTESIAN_POINT('Origin',(0.,0.03,0.));
#6143=CARTESIAN_POINT('',(-0.35,0.19,-4.28626379701574E-17));
#6144=CARTESIAN_POINT('Origin',(0.,0.0149999999999999,0.));
#6145=CARTESIAN_POINT('',(-0.32,-3.29597460435593E-17,-3.91886975727153E-17));
#6146=CARTESIAN_POINT('Origin',(0.,0.,0.));
#6147=CARTESIAN_POINT('',(-0.335,0.0149999999999999,-4.10256677714363E-17));
#6148=CARTESIAN_POINT('Origin',(0.22,0.,0.));
#6149=CARTESIAN_POINT('',(-0.22,-6.93889390390723E-18,-2.69422295812418E-17));
#6150=CARTESIAN_POINT('Origin',(0.,0.,0.));
#6151=CARTESIAN_POINT('Origin',(0.,-0.02,0.));
#6152=CARTESIAN_POINT('',(-0.1954,-0.0492,2.39295984553393E-17));
#6153=CARTESIAN_POINT('Origin',(0.,-0.0492,0.));
#6154=CARTESIAN_POINT('',(-0.21,-0.02,-2.57175827820944E-17));
#6155=CARTESIAN_POINT('Origin',(0.,-0.8,0.));
#6156=CARTESIAN_POINT('',(-0.1954,-1.5646,2.39295984553393E-17));
#6157=CARTESIAN_POINT('Origin',(0.,-1.5646,0.));
#6158=CARTESIAN_POINT('',(-0.1954,-0.8,-2.39295984553393E-17));
#6159=CARTESIAN_POINT('Origin',(0.,-1.58,0.));
#6160=CARTESIAN_POINT('',(-0.16,-1.6,-1.95943487863577E-17));
#6161=CARTESIAN_POINT('Origin',(0.,-1.6,0.));
#6162=CARTESIAN_POINT('',(-0.18,-1.58,-2.20436423846524E-17));
#6163=CARTESIAN_POINT('Origin',(0.,-1.6,0.));
#6164=CARTESIAN_POINT('Origin',(0.0866025403784439,-0.4,-0.15));
#6165=CARTESIAN_POINT('',(0.173205080756888,-0.4,0.));
#6166=CARTESIAN_POINT('',(0.0866025403784439,-0.4,-0.15));
#6167=CARTESIAN_POINT('',(0.173205080756888,-0.4,0.));
#6168=CARTESIAN_POINT('',(0.0866025403784439,-0.64,-0.15));
#6169=CARTESIAN_POINT('',(0.0866025403784439,-0.4,-0.15));
#6170=CARTESIAN_POINT('',(0.173205080756888,-0.64,0.));
#6171=CARTESIAN_POINT('',(0.173205080756888,-0.64,0.));
#6172=CARTESIAN_POINT('',(0.173205080756888,-0.4,0.));
#6173=CARTESIAN_POINT('Origin',(-0.0866025403784438,-0.4,-0.15));
#6174=CARTESIAN_POINT('',(-0.0866025403784438,-0.4,-0.15));
#6175=CARTESIAN_POINT('',(0.0866025403784439,-0.4,-0.15));
#6176=CARTESIAN_POINT('',(-0.0866025403784438,-0.64,-0.15));
#6177=CARTESIAN_POINT('',(-0.0866025403784438,-0.4,-0.15));
#6178=CARTESIAN_POINT('',(0.0866025403784439,-0.64,-0.15));
#6179=CARTESIAN_POINT('Origin',(-0.173205080756888,-0.4,-2.77555756156289E-17));
#6180=CARTESIAN_POINT('',(-0.173205080756888,-0.4,-2.12115047744981E-17));
#6181=CARTESIAN_POINT('',(-0.0866025403784438,-0.4,-0.15));
#6182=CARTESIAN_POINT('',(-0.173205080756888,-0.64,-2.77555756156289E-17));
#6183=CARTESIAN_POINT('',(-0.173205080756888,-0.4,-2.12115047744981E-17));
#6184=CARTESIAN_POINT('',(-0.0866025403784438,-0.64,-0.15));
#6185=CARTESIAN_POINT('Origin',(-0.0866025403784439,-0.4,0.15));
#6186=CARTESIAN_POINT('',(-0.0866025403784439,-0.4,0.15));
#6187=CARTESIAN_POINT('',(-0.173205080756888,-0.4,-2.12115047744981E-17));
#6188=CARTESIAN_POINT('',(-0.0866025403784439,-0.64,0.15));
#6189=CARTESIAN_POINT('',(-0.0866025403784439,-0.4,0.15));
#6190=CARTESIAN_POINT('',(-0.173205080756888,-0.64,-2.12115047744981E-17));
#6191=CARTESIAN_POINT('Origin',(0.0866025403784439,-0.4,0.15));
#6192=CARTESIAN_POINT('',(0.0866025403784439,-0.4,0.15));
#6193=CARTESIAN_POINT('',(-0.0866025403784439,-0.4,0.15));
#6194=CARTESIAN_POINT('',(0.0866025403784439,-0.64,0.15));
#6195=CARTESIAN_POINT('',(0.0866025403784439,-0.4,0.15));
#6196=CARTESIAN_POINT('',(-0.0866025403784439,-0.64,0.15));
#6197=CARTESIAN_POINT('Origin',(0.173205080756888,-0.4,0.));
#6198=CARTESIAN_POINT('',(0.0866025403784439,-0.4,0.15));
#6199=CARTESIAN_POINT('',(0.0866025403784439,-0.64,0.15));
#6200=CARTESIAN_POINT('Origin',(0.,-0.4,-2.77555756156289E-17));
#6201=CARTESIAN_POINT('Origin',(0.,-0.64,-2.77555756156289E-17));
#6437=UNCERTAINTY_MEASURE_WITH_UNIT(LENGTH_MEASURE(0.001),#6464,
'DISTANCE_ACCURACY_VALUE',
'Maximum model space distance between geometric entities at asserted c
onnectivities');
#6442=UNCERTAINTY_MEASURE_WITH_UNIT(LENGTH_MEASURE(0.001),#6464,
'DISTANCE_ACCURACY_VALUE',
'Maximum model space distance between geometric entities at asserted c
onnectivities');
#6458=(
GEOMETRIC_REPRESENTATION_CONTEXT(3)
GLOBAL_UNCERTAINTY_ASSIGNED_CONTEXT((#6437))
GLOBAL_UNIT_ASSIGNED_CONTEXT((#6464,#6466,#6467))
REPRESENTATION_CONTEXT('','3D')
);
#6463=(
GEOMETRIC_REPRESENTATION_CONTEXT(3)
GLOBAL_UNCERTAINTY_ASSIGNED_CONTEXT((#6442))
GLOBAL_UNIT_ASSIGNED_CONTEXT((#6464,#6466,#6467))
REPRESENTATION_CONTEXT('','3D')
);
#6464=(
LENGTH_UNIT()
NAMED_UNIT(*)
SI_UNIT(.CENTI.,.METRE.)
);
#6466=(
NAMED_UNIT(*)
PLANE_ANGLE_UNIT()
SI_UNIT($,.RADIAN.)
);
#6467=(
NAMED_UNIT(*)
SI_UNIT($,.STERADIAN.)
SOLID_ANGLE_UNIT()
);
#6483=SHAPE_DEFINITION_REPRESENTATION(#6505,#6575);
#6505=PRODUCT_DEFINITION_SHAPE('',$,#6596);
#6575=SHAPE_REPRESENTATION('',(#4121),#6458);
#6580=PRODUCT_DEFINITION_CONTEXT('part definition',#6642,'design');
#6596=PRODUCT_DEFINITION('Cap Screw - M4x16','Cap Screw - M4x16',#6616,
#6580);
#6616=PRODUCT_DEFINITION_FORMATION('',$,#6659);
#6642=APPLICATION_CONTEXT(
'Core Data for Automotive Mechanical Design Process');
#6643=PRODUCT_CONTEXT('part definition',#6642,'mechanical');
#6659=PRODUCT('Cap Screw - M4x16','Cap Screw - M4x16',
'Cap Screw - M4x16',(#6643));
#6741=COLOUR_RGB('Black',0.12,0.14,0.17);
#6742=FILL_AREA_STYLE_COLOUR('',#6741);
#6743=FILL_AREA_STYLE('',(#6742));
#6744=SURFACE_STYLE_FILL_AREA(#6743);
#6745=SURFACE_SIDE_STYLE('',(#6744));
#6746=SURFACE_STYLE_USAGE(.BOTH.,#6745);
#6747=PRESENTATION_STYLE_ASSIGNMENT((#6746));
ENDSEC;
END-ISO-10303-21;
